ISO-10303-21;
HEADER;
/* Generated by software containing ST-Developer
 * from STEP Tools, Inc. (www.steptools.com) 
 */

FILE_DESCRIPTION(
/* description */ ('Counter shaft with two pulleys and keyed hub'),
/* implementation_level */ '2;1');

FILE_NAME(
/* name */ 'Flat Washer - M8.step',
/* time_stamp */ '2026-10-27T10:46:10-07:00',
/* author */ (''),
/* organization */ (''),
/* preprocessor_version */ 'ST-DEVELOPER v20.2',
/* originating_system */ 'Autodesk Translation Framework v15.17.0.0',
/* authorisation */ '');

FILE_SCHEMA (('AUTOMOTIVE_DESIGN { 1 0 10303 214 3 1 1 }'));
ENDSEC;

DATA;
#10=MECHANICAL_DESIGN_GEOMETRIC_PRESENTATION_REPRESENTATION('',(#300),#10821);
#249=SHAPE_REPRESENTATION_RELATIONSHIP('SRR','None',#10936,#274);
#274=ADVANCED_BREP_SHAPE_REPRESENTATION('',(#326),#10804);
#300=STYLED_ITEM('',(#11142),#326);
#326=MANIFOLD_SOLID_BREP('Body1',#5583);
#385=FACE_BOUND('',#1029,.T.);
#386=FACE_BOUND('',#1031,.T.);
#481=PLANE('',#6027);
#482=PLANE('',#6028);
#667=FACE_OUTER_BOUND('',#1026,.T.);
#668=FACE_OUTER_BOUND('',#1027,.T.);
#669=FACE_OUTER_BOUND('',#1028,.T.);
#670=FACE_OUTER_BOUND('',#1030,.T.);
#1026=EDGE_LOOP('',(#3985,#3986,#3987,#3988));
#1027=EDGE_LOOP('',(#3989,#3990,#3991,#3992));
#1028=EDGE_LOOP('',(#3993));
#1029=EDGE_LOOP('',(#3994));
#1030=EDGE_LOOP('',(#3995));
#1031=EDGE_LOOP('',(#3996));
#1411=LINE('',#9122,#1800);
#1412=LINE('',#9128,#1801);
#1800=VECTOR('',#6955,0.42);
#1801=VECTOR('',#6962,0.8);
#2135=CIRCLE('',#6022,0.42);
#2136=CIRCLE('',#6023,0.42);
#2137=CIRCLE('',#6025,0.8);
#2138=CIRCLE('',#6026,0.8);
#2510=VERTEX_POINT('',#9119);
#2511=VERTEX_POINT('',#9121);
#2512=VERTEX_POINT('',#9125);
#2513=VERTEX_POINT('',#9127);
#3065=EDGE_CURVE('',#2510,#2510,#2135,.T.);
#3066=EDGE_CURVE('',#2510,#2511,#1411,.T.);
#3067=EDGE_CURVE('',#2511,#2511,#2136,.T.);
#3068=EDGE_CURVE('',#2512,#2512,#2137,.T.);
#3069=EDGE_CURVE('',#2512,#2513,#1412,.T.);
#3070=EDGE_CURVE('',#2513,#2513,#2138,.T.);
#3985=ORIENTED_EDGE('',*,*,#3065,.F.);
#3986=ORIENTED_EDGE('',*,*,#3066,.T.);
#3987=ORIENTED_EDGE('',*,*,#3067,.T.);
#3988=ORIENTED_EDGE('',*,*,#3066,.F.);
#3989=ORIENTED_EDGE('',*,*,#3068,.F.);
#3990=ORIENTED_EDGE('',*,*,#3069,.T.);
#3991=ORIENTED_EDGE('',*,*,#3070,.T.);
#3992=ORIENTED_EDGE('',*,*,#3069,.F.);
#3993=ORIENTED_EDGE('',*,*,#3068,.T.);
#3994=ORIENTED_EDGE('',*,*,#3065,.T.);
#3995=ORIENTED_EDGE('',*,*,#3070,.F.);
#3996=ORIENTED_EDGE('',*,*,#3067,.F.);
#5140=CYLINDRICAL_SURFACE('',#6021,0.42);
#5141=CYLINDRICAL_SURFACE('',#6024,0.8);
#5338=ADVANCED_FACE('',(#667),#5140,.F.);
#5339=ADVANCED_FACE('',(#668),#5141,.T.);
#5340=ADVANCED_FACE('',(#669,#385),#481,.T.);
#5341=ADVANCED_FACE('',(#670,#386),#482,.F.);
#5583=CLOSED_SHELL('',(#5338,#5339,#5340,#5341));
#6020=AXIS2_PLACEMENT_3D('',#9117,#6949,#6950);
#6021=AXIS2_PLACEMENT_3D('',#9118,#6951,#6952);
#6022=AXIS2_PLACEMENT_3D('',#9120,#6953,#6954);
#6023=AXIS2_PLACEMENT_3D('',#9123,#6956,#6957);
#6024=AXIS2_PLACEMENT_3D('',#9124,#6958,#6959);
#6025=AXIS2_PLACEMENT_3D('',#9126,#6960,#6961);
#6026=AXIS2_PLACEMENT_3D('',#9129,#6963,#6964);
#6027=AXIS2_PLACEMENT_3D('',#9130,#6965,#6966);
#6028=AXIS2_PLACEMENT_3D('',#9131,#6967,#6968);
#6949=DIRECTION('axis',(0.,0.,1.));
#6950=DIRECTION('refdir',(1.,0.,0.));
#6951=DIRECTION('center_axis',(0.,1.,0.));
#6952=DIRECTION('ref_axis',(1.,0.,0.));
#6953=DIRECTION('center_axis',(0.,-1.,0.));
#6954=DIRECTION('ref_axis',(1.,0.,0.));
#6955=DIRECTION('',(0.,-1.,0.));
#6956=DIRECTION('center_axis',(0.,-1.,0.));
#6957=DIRECTION('ref_axis',(1.,0.,0.));
#6958=DIRECTION('center_axis',(0.,1.,0.));
#6959=DIRECTION('ref_axis',(1.,0.,0.));
#6960=DIRECTION('center_axis',(0.,1.,0.));
#6961=DIRECTION('ref_axis',(1.,0.,0.));
#6962=DIRECTION('',(0.,-1.,0.));
#6963=DIRECTION('center_axis',(0.,1.,0.));
#6964=DIRECTION('ref_axis',(1.,0.,0.));
#6965=DIRECTION('center_axis',(0.,1.,0.));
#6966=DIRECTION('ref_axis',(1.,0.,0.));
#6967=DIRECTION('center_axis',(0.,1.,0.));
#6968=DIRECTION('ref_axis',(1.,0.,0.));
#9117=CARTESIAN_POINT('',(0.,0.,0.));
#9118=CARTESIAN_POINT('Origin',(0.,0.,0.));
#9119=CARTESIAN_POINT('',(-0.42,0.16,5.14351655641888E-17));
#9120=CARTESIAN_POINT('Origin',(0.,0.16,0.));
#9121=CARTESIAN_POINT('',(-0.42,0.,5.14351655641888E-17));
#9122=CARTESIAN_POINT('',(-0.42,0.,5.14351655641888E-17));
#9123=CARTESIAN_POINT('Origin',(0.,0.,0.));
#9124=CARTESIAN_POINT('Origin',(0.,0.,0.));
#9125=CARTESIAN_POINT('',(-0.8,0.16,9.79717439317883E-17));
#9126=CARTESIAN_POINT('Origin',(0.,0.16,0.));
#9127=CARTESIAN_POINT('',(-0.8,0.,9.79717439317883E-17));
#9128=CARTESIAN_POINT('',(-0.8,0.,9.79717439317883E-17));
#9129=CARTESIAN_POINT('Origin',(0.,0.,0.));
#9130=CARTESIAN_POINT('Origin',(0.,0.16,0.));
#9131=CARTESIAN_POINT('Origin',(0.,0.,0.));
#10774=UNCERTAINTY_MEASURE_WITH_UNIT(LENGTH_MEASURE(0.001),#10822,
'DISTANCE_ACCURACY_VALUE',
'Maximum model space distance between geometric entities at asserted c
onnectivities');
#10791=UNCERTAINTY_MEASURE_WITH_UNIT(LENGTH_MEASURE(0.001),#10822,
'DISTANCE_ACCURACY_VALUE',
'Maximum model space distance between geometric entities at asserted c
onnectivities');
#10804=(
GEOMETRIC_REPRESENTATION_CONTEXT(3)
GLOBAL_UNCERTAINTY_ASSIGNED_CONTEXT((#10774))
GLOBAL_UNIT_ASSIGNED_CONTEXT((#10822,#10824,#10825))
REPRESENTATION_CONTEXT('','3D')
);
#10821=(
GEOMETRIC_REPRESENTATION_CONTEXT(3)
GLOBAL_UNCERTAINTY_ASSIGNED_CONTEXT((#10791))
GLOBAL_UNIT_ASSIGNED_CONTEXT((#10822,#10824,#10825))
REPRESENTATION_CONTEXT('','3D')
);
#10822=(
LENGTH_UNIT()
NAMED_UNIT(*)
SI_UNIT(.CENTI.,.METRE.)
);
#10824=(
NAMED_UNIT(*)
PLANE_ANGLE_UNIT()
SI_UNIT($,.RADIAN.)
);
#10825=(
NAMED_UNIT(*)
SI_UNIT($,.STERADIAN.)
SOLID_ANGLE_UNIT()
);
#10838=SHAPE_DEFINITION_REPRESENTATION(#10869,#10936);
#10869=PRODUCT_DEFINITION_SHAPE('',$,#10966);
#10936=SHAPE_REPRESENTATION('',(#6020),#10804);
#10953=PRODUCT_DEFINITION_CONTEXT('part definition',#11042,'design');
#10966=PRODUCT_DEFINITION('Flat Washer - M8','Flat Washer - M8',#10995,
#10953);
#10995=PRODUCT_DEFINITION_FORMATION('',$,#11056);
#11042=APPLICATION_CONTEXT(
'Core Data for Automotive Mechanical Design Process');
#11043=PRODUCT_CONTEXT('part definition',#11042,'mechanical');
#11056=PRODUCT('Flat Washer - M8','Flat Washer - M8','Flat Washer - M8',
(#11043));
#11136=COLOUR_RGB('Black',0.12,0.14,0.17);
#11137=FILL_AREA_STYLE_COLOUR('',#11136);
#11138=FILL_AREA_STYLE('',(#11137));
#11139=SURFACE_STYLE_FILL_AREA(#11138);
#11140=SURFACE_SIDE_STYLE('',(#11139));
#11141=SURFACE_STYLE_USAGE(.BOTH.,#11140);
#11142=PRESENTATION_STYLE_ASSIGNMENT((#11141));
ENDSEC;
END-ISO-10303-21;
